ISO-10303-21;
HEADER;
/* Generated by software containing ST-Developer
 * from STEP Tools, Inc. (www.steptools.com) 
 */

FILE_DESCRIPTION(
/* description */ ('Located fixture plate with toggle clamp'),
/* implementation_level */ '2;1');

FILE_NAME(
/* name */ 'Hex Bolt - M8x40.step',
/* time_stamp */ '2026-10-27T21:36:12-07:00',
/* author */ (''),
/* organization */ (''),
/* preprocessor_version */ 'ST-DEVELOPER v20.2',
/* originating_system */ 'Autodesk Translation Framework v15.17.0.0',
/* authorisation */ '');

FILE_SCHEMA (('AUTOMOTIVE_DESIGN { 1 0 10303 214 3 1 1 }'));
ENDSEC;

DATA;
#10=MECHANICAL_DESIGN_GEOMETRIC_PRESENTATION_REPRESENTATION('',(#338),#9285);
#226=(
BOUNDED_CURVE()
B_SPLINE_CURVE(2,(#8838,#8839,#8840),.UNSPECIFIED.,.F.,.F.)
B_SPLINE_CURVE_WITH_KNOTS((3,3),(0.14973948338295,0.97160236658079),
 .UNSPECIFIED.)
CURVE()
GEOMETRIC_REPRESENTATION_ITEM()
RATIONAL_B_SPLINE_CURVE((1.07140024848292,1.23714644374248,1.07140024848292))
REPRESENTATION_ITEM('')
);
#227=(
BOUNDED_CURVE()
B_SPLINE_CURVE(2,(#8842,#8843,#8844),.UNSPECIFIED.,.F.,.F.)
B_SPLINE_CURVE_WITH_KNOTS((3,3),(0.14973948338295,0.97160236658079),
 .UNSPECIFIED.)
CURVE()
GEOMETRIC_REPRESENTATION_ITEM()
RATIONAL_B_SPLINE_CURVE((1.07140024848292,1.23714644374248,1.07140024848292))
REPRESENTATION_ITEM('')
);
#228=(
BOUNDED_CURVE()
B_SPLINE_CURVE(2,(#8846,#8847,#8848),.UNSPECIFIED.,.F.,.F.)
B_SPLINE_CURVE_WITH_KNOTS((3,3),(0.14973948338295,0.97160236658079),
 .UNSPECIFIED.)
CURVE()
GEOMETRIC_REPRESENTATION_ITEM()
RATIONAL_B_SPLINE_CURVE((1.07140024848292,1.23714644374248,1.07140024848292))
REPRESENTATION_ITEM('')
);
#229=(
BOUNDED_CURVE()
B_SPLINE_CURVE(2,(#8850,#8851,#8852),.UNSPECIFIED.,.F.,.F.)
B_SPLINE_CURVE_WITH_KNOTS((3,3),(0.149739483382949,0.971602366580789),
 .UNSPECIFIED.)
CURVE()
GEOMETRIC_REPRESENTATION_ITEM()
RATIONAL_B_SPLINE_CURVE((1.07140024848292,1.23714644374248,1.07140024848292))
REPRESENTATION_ITEM('')
);
#230=(
BOUNDED_CURVE()
B_SPLINE_CURVE(2,(#8854,#8855,#8856),.UNSPECIFIED.,.F.,.F.)
B_SPLINE_CURVE_WITH_KNOTS((3,3),(0.14973948338295,0.971602366580789),
 .UNSPECIFIED.)
CURVE()
GEOMETRIC_REPRESENTATION_ITEM()
RATIONAL_B_SPLINE_CURVE((1.07140024848292,1.23714644374248,1.07140024848292))
REPRESENTATION_ITEM('')
);
#231=(
BOUNDED_CURVE()
B_SPLINE_CURVE(2,(#8857,#8858,#8859),.UNSPECIFIED.,.F.,.F.)
B_SPLINE_CURVE_WITH_KNOTS((3,3),(0.14973948338295,0.97160236658079),
 .UNSPECIFIED.)
CURVE()
GEOMETRIC_REPRESENTATION_ITEM()
RATIONAL_B_SPLINE_CURVE((1.07140024848292,1.23714644374248,1.07140024848292))
REPRESENTATION_ITEM('')
);
#267=CONICAL_SURFACE('',#5905,0.36,0.785398163397451);
#268=CONICAL_SURFACE('',#5908,0.734027674973257,1.0471975511966);
#290=SHAPE_REPRESENTATION_RELATIONSHIP('SRR','None',#9416,#314);
#314=ADVANCED_BREP_SHAPE_REPRESENTATION('',(#359),#9278);
#338=STYLED_ITEM('',(#9619),#359);
#359=MANIFOLD_SOLID_BREP('Body1',#5189);
#476=FACE_BOUND('',#1338,.T.);
#644=PLANE('',#5907);
#645=PLANE('',#5910);
#646=PLANE('',#5911);
#647=PLANE('',#5912);
#648=PLANE('',#5913);
#649=PLANE('',#5914);
#650=PLANE('',#5915);
#651=PLANE('',#5916);
#652=PLANE('',#5917);
#921=FACE_OUTER_BOUND('',#1326,.T.);
#922=FACE_OUTER_BOUND('',#1327,.T.);
#923=FACE_OUTER_BOUND('',#1328,.T.);
#924=FACE_OUTER_BOUND('',#1329,.T.);
#925=FACE_OUTER_BOUND('',#1330,.T.);
#926=FACE_OUTER_BOUND('',#1331,.T.);
#927=FACE_OUTER_BOUND('',#1332,.T.);
#928=FACE_OUTER_BOUND('',#1333,.T.);
#929=FACE_OUTER_BOUND('',#1334,.T.);
#930=FACE_OUTER_BOUND('',#1335,.T.);
#931=FACE_OUTER_BOUND('',#1336,.T.);
#932=FACE_OUTER_BOUND('',#1337,.T.);
#1326=EDGE_LOOP('',(#4606,#4607,#4608,#4609));
#1327=EDGE_LOOP('',(#4610,#4611,#4612,#4613));
#1328=EDGE_LOOP('',(#4614));
#1329=EDGE_LOOP('',(#4615,#4616,#4617,#4618,#4619,#4620,#4621,#4622,#4623));
#1330=EDGE_LOOP('',(#4624,#4625,#4626,#4627));
#1331=EDGE_LOOP('',(#4628,#4629,#4630,#4631));
#1332=EDGE_LOOP('',(#4632,#4633,#4634,#4635));
#1333=EDGE_LOOP('',(#4636,#4637,#4638,#4639));
#1334=EDGE_LOOP('',(#4640,#4641,#4642,#4643));
#1335=EDGE_LOOP('',(#4644,#4645,#4646,#4647));
#1336=EDGE_LOOP('',(#4648));
#1337=EDGE_LOOP('',(#4649,#4650,#4651,#4652,#4653,#4654));
#1338=EDGE_LOOP('',(#4655));
#1552=CIRCLE('',#5903,0.3933);
#1553=CIRCLE('',#5904,0.3933);
#1554=CIRCLE('',#5906,0.32);
#1555=CIRCLE('',#5909,0.6175);
#1951=LINE('',#8825,#2361);
#1952=LINE('',#8830,#2362);
#1953=LINE('',#8836,#2363);
#1954=LINE('',#8862,#2364);
#1955=LINE('',#8864,#2365);
#1956=LINE('',#8865,#2366);
#1957=LINE('',#8868,#2367);
#1958=LINE('',#8869,#2368);
#1959=LINE('',#8872,#2369);
#1960=LINE('',#8873,#2370);
#1961=LINE('',#8876,#2371);
#1962=LINE('',#8877,#2372);
#1963=LINE('',#8880,#2373);
#1964=LINE('',#8881,#2374);
#1965=LINE('',#8883,#2375);
#2361=VECTOR('',#7285,0.4);
#2362=VECTOR('',#7292,0.36);
#2363=VECTOR('',#7299,0.734027674973257);
#2364=VECTOR('',#7302,1.);
#2365=VECTOR('',#7303,1.);
#2366=VECTOR('',#7304,1.);
#2367=VECTOR('',#7307,1.);
#2368=VECTOR('',#7308,1.);
#2369=VECTOR('',#7311,1.);
#2370=VECTOR('',#7312,1.);
#2371=VECTOR('',#7315,1.);
#2372=VECTOR('',#7316,1.);
#2373=VECTOR('',#7319,1.);
#2374=VECTOR('',#7320,1.);
#2375=VECTOR('',#7323,1.);
#2770=VERTEX_POINT('',#8822);
#2771=VERTEX_POINT('',#8824);
#2772=VERTEX_POINT('',#8828);
#2773=VERTEX_POINT('',#8833);
#2774=VERTEX_POINT('',#8835);
#2775=VERTEX_POINT('',#8837);
#2776=VERTEX_POINT('',#8841);
#2777=VERTEX_POINT('',#8845);
#2778=VERTEX_POINT('',#8849);
#2779=VERTEX_POINT('',#8853);
#2780=VERTEX_POINT('',#8861);
#2781=VERTEX_POINT('',#8863);
#2782=VERTEX_POINT('',#8867);
#2783=VERTEX_POINT('',#8871);
#2784=VERTEX_POINT('',#8875);
#2785=VERTEX_POINT('',#8879);
#3391=EDGE_CURVE('',#2770,#2770,#1552,.F.);
#3392=EDGE_CURVE('',#2770,#2771,#1951,.T.);
#3393=EDGE_CURVE('',#2771,#2771,#1553,.F.);
#3394=EDGE_CURVE('',#2772,#2772,#1554,.T.);
#3395=EDGE_CURVE('',#2772,#2770,#1952,.T.);
#3396=EDGE_CURVE('',#2773,#2773,#1555,.T.);
#3397=EDGE_CURVE('',#2773,#2774,#1953,.T.);
#3398=EDGE_CURVE('',#2775,#2774,#226,.T.);
#3399=EDGE_CURVE('',#2776,#2775,#227,.T.);
#3400=EDGE_CURVE('',#2777,#2776,#228,.T.);
#3401=EDGE_CURVE('',#2778,#2777,#229,.T.);
#3402=EDGE_CURVE('',#2779,#2778,#230,.T.);
#3403=EDGE_CURVE('',#2774,#2779,#231,.T.);
#3404=EDGE_CURVE('',#2780,#2778,#1954,.T.);
#3405=EDGE_CURVE('',#2780,#2781,#1955,.T.);
#3406=EDGE_CURVE('',#2781,#2779,#1956,.T.);
#3407=EDGE_CURVE('',#2782,#2777,#1957,.T.);
#3408=EDGE_CURVE('',#2782,#2780,#1958,.T.);
#3409=EDGE_CURVE('',#2783,#2776,#1959,.T.);
#3410=EDGE_CURVE('',#2783,#2782,#1960,.T.);
#3411=EDGE_CURVE('',#2784,#2775,#1961,.T.);
#3412=EDGE_CURVE('',#2784,#2783,#1962,.T.);
#3413=EDGE_CURVE('',#2785,#2774,#1963,.T.);
#3414=EDGE_CURVE('',#2785,#2784,#1964,.T.);
#3415=EDGE_CURVE('',#2781,#2785,#1965,.T.);
#4606=ORIENTED_EDGE('',*,*,#3391,.F.);
#4607=ORIENTED_EDGE('',*,*,#3392,.T.);
#4608=ORIENTED_EDGE('',*,*,#3393,.F.);
#4609=ORIENTED_EDGE('',*,*,#3392,.F.);
#4610=ORIENTED_EDGE('',*,*,#3394,.F.);
#4611=ORIENTED_EDGE('',*,*,#3395,.T.);
#4612=ORIENTED_EDGE('',*,*,#3391,.T.);
#4613=ORIENTED_EDGE('',*,*,#3395,.F.);
#4614=ORIENTED_EDGE('',*,*,#3394,.T.);
#4615=ORIENTED_EDGE('',*,*,#3396,.F.);
#4616=ORIENTED_EDGE('',*,*,#3397,.T.);
#4617=ORIENTED_EDGE('',*,*,#3398,.F.);
#4618=ORIENTED_EDGE('',*,*,#3399,.F.);
#4619=ORIENTED_EDGE('',*,*,#3400,.F.);
#4620=ORIENTED_EDGE('',*,*,#3401,.F.);
#4621=ORIENTED_EDGE('',*,*,#3402,.F.);
#4622=ORIENTED_EDGE('',*,*,#3403,.F.);
#4623=ORIENTED_EDGE('',*,*,#3397,.F.);
#4624=ORIENTED_EDGE('',*,*,#3402,.T.);
#4625=ORIENTED_EDGE('',*,*,#3404,.F.);
#4626=ORIENTED_EDGE('',*,*,#3405,.T.);
#4627=ORIENTED_EDGE('',*,*,#3406,.T.);
#4628=ORIENTED_EDGE('',*,*,#3401,.T.);
#4629=ORIENTED_EDGE('',*,*,#3407,.F.);
#4630=ORIENTED_EDGE('',*,*,#3408,.T.);
#4631=ORIENTED_EDGE('',*,*,#3404,.T.);
#4632=ORIENTED_EDGE('',*,*,#3400,.T.);
#4633=ORIENTED_EDGE('',*,*,#3409,.F.);
#4634=ORIENTED_EDGE('',*,*,#3410,.T.);
#4635=ORIENTED_EDGE('',*,*,#3407,.T.);
#4636=ORIENTED_EDGE('',*,*,#3399,.T.);
#4637=ORIENTED_EDGE('',*,*,#3411,.F.);
#4638=ORIENTED_EDGE('',*,*,#3412,.T.);
#4639=ORIENTED_EDGE('',*,*,#3409,.T.);
#4640=ORIENTED_EDGE('',*,*,#3398,.T.);
#4641=ORIENTED_EDGE('',*,*,#3413,.F.);
#4642=ORIENTED_EDGE('',*,*,#3414,.T.);
#4643=ORIENTED_EDGE('',*,*,#3411,.T.);
#4644=ORIENTED_EDGE('',*,*,#3403,.T.);
#4645=ORIENTED_EDGE('',*,*,#3406,.F.);
#4646=ORIENTED_EDGE('',*,*,#3415,.T.);
#4647=ORIENTED_EDGE('',*,*,#3413,.T.);
#4648=ORIENTED_EDGE('',*,*,#3396,.T.);
#4649=ORIENTED_EDGE('',*,*,#3410,.F.);
#4650=ORIENTED_EDGE('',*,*,#3412,.F.);
#4651=ORIENTED_EDGE('',*,*,#3414,.F.);
#4652=ORIENTED_EDGE('',*,*,#3415,.F.);
#4653=ORIENTED_EDGE('',*,*,#3405,.F.);
#4654=ORIENTED_EDGE('',*,*,#3408,.F.);
#4655=ORIENTED_EDGE('',*,*,#3393,.T.);
#4863=CYLINDRICAL_SURFACE('',#5902,0.3933);
#5122=ADVANCED_FACE('',(#921),#4863,.T.);
#5123=ADVANCED_FACE('',(#922),#267,.T.);
#5124=ADVANCED_FACE('',(#923),#644,.T.);
#5125=ADVANCED_FACE('',(#924),#268,.T.);
#5126=ADVANCED_FACE('',(#925),#645,.T.);
#5127=ADVANCED_FACE('',(#926),#646,.T.);
#5128=ADVANCED_FACE('',(#927),#647,.T.);
#5129=ADVANCED_FACE('',(#928),#648,.T.);
#5130=ADVANCED_FACE('',(#929),#649,.T.);
#5131=ADVANCED_FACE('',(#930),#650,.T.);
#5132=ADVANCED_FACE('',(#931),#651,.T.);
#5133=ADVANCED_FACE('',(#932,#476),#652,.F.);
#5189=CLOSED_SHELL('',(#5122,#5123,#5124,#5125,#5126,#5127,#5128,#5129,
#5130,#5131,#5132,#5133));
#5901=AXIS2_PLACEMENT_3D('',#8820,#7279,#7280);
#5902=AXIS2_PLACEMENT_3D('',#8821,#7281,#7282);
#5903=AXIS2_PLACEMENT_3D('',#8823,#7283,#7284);
#5904=AXIS2_PLACEMENT_3D('',#8826,#7286,#7287);
#5905=AXIS2_PLACEMENT_3D('',#8827,#7288,#7289);
#5906=AXIS2_PLACEMENT_3D('',#8829,#7290,#7291);
#5907=AXIS2_PLACEMENT_3D('',#8831,#7293,#7294);
#5908=AXIS2_PLACEMENT_3D('',#8832,#7295,#7296);
#5909=AXIS2_PLACEMENT_3D('',#8834,#7297,#7298);
#5910=AXIS2_PLACEMENT_3D('',#8860,#7300,#7301);
#5911=AXIS2_PLACEMENT_3D('',#8866,#7305,#7306);
#5912=AXIS2_PLACEMENT_3D('',#8870,#7309,#7310);
#5913=AXIS2_PLACEMENT_3D('',#8874,#7313,#7314);
#5914=AXIS2_PLACEMENT_3D('',#8878,#7317,#7318);
#5915=AXIS2_PLACEMENT_3D('',#8882,#7321,#7322);
#5916=AXIS2_PLACEMENT_3D('',#8884,#7324,#7325);
#5917=AXIS2_PLACEMENT_3D('',#8885,#7326,#7327);
#7279=DIRECTION('axis',(0.,0.,1.));
#7280=DIRECTION('refdir',(1.,0.,0.));
#7281=DIRECTION('center_axis',(0.,-1.,0.));
#7282=DIRECTION('ref_axis',(1.,0.,0.));
#7283=DIRECTION('center_axis',(0.,1.,0.));
#7284=DIRECTION('ref_axis',(1.,0.,0.));
#7285=DIRECTION('',(0.,1.,0.));
#7286=DIRECTION('center_axis',(0.,-1.,0.));
#7287=DIRECTION('ref_axis',(1.,0.,0.));
#7288=DIRECTION('center_axis',(0.,1.,0.));
#7289=DIRECTION('ref_axis',(1.,0.,0.));
#7290=DIRECTION('center_axis',(0.,-1.,0.));
#7291=DIRECTION('ref_axis',(1.,0.,0.));
#7292=DIRECTION('',(-0.707106781186549,0.707106781186546,-8.65956056235496E-17));
#7293=DIRECTION('center_axis',(0.,-1.,0.));
#7294=DIRECTION('ref_axis',(0.,0.,-1.));
#7295=DIRECTION('center_axis',(0.,-1.,0.));
#7296=DIRECTION('ref_axis',(1.,0.,0.));
#7297=DIRECTION('center_axis',(0.,1.,0.));
#7298=DIRECTION('ref_axis',(1.,0.,0.));
#7299=DIRECTION('',(-0.866025403784439,-0.5,-1.06057523872491E-16));
#7300=DIRECTION('center_axis',(1.4792020664489E-16,0.,-1.));
#7301=DIRECTION('ref_axis',(-1.,0.,-1.4792020664489E-16));
#7302=DIRECTION('',(0.,1.,0.));
#7303=DIRECTION('',(-1.,0.,-1.4792020664489E-16));
#7304=DIRECTION('',(0.,1.,0.));
#7305=DIRECTION('center_axis',(0.866025403784439,0.,-0.5));
#7306=DIRECTION('ref_axis',(-0.5,0.,-0.866025403784439));
#7307=DIRECTION('',(0.,1.,0.));
#7308=DIRECTION('',(-0.5,0.,-0.866025403784439));
#7309=DIRECTION('center_axis',(0.866025403784439,0.,0.5));
#7310=DIRECTION('ref_axis',(0.5,0.,-0.866025403784439));
#7311=DIRECTION('',(0.,1.,0.));
#7312=DIRECTION('',(0.5,0.,-0.866025403784439));
#7313=DIRECTION('center_axis',(-2.95840413289779E-16,0.,1.));
#7314=DIRECTION('ref_axis',(1.,0.,2.95840413289779E-16));
#7315=DIRECTION('',(0.,1.,0.));
#7316=DIRECTION('',(1.,0.,2.95840413289779E-16));
#7317=DIRECTION('center_axis',(-0.866025403784439,0.,0.5));
#7318=DIRECTION('ref_axis',(0.5,0.,0.866025403784439));
#7319=DIRECTION('',(0.,1.,0.));
#7320=DIRECTION('',(0.5,0.,0.866025403784439));
#7321=DIRECTION('center_axis',(-0.866025403784439,0.,-0.5));
#7322=DIRECTION('ref_axis',(-0.5,0.,0.866025403784439));
#7323=DIRECTION('',(-0.5,0.,0.866025403784439));
#7324=DIRECTION('center_axis',(0.,1.,0.));
#7325=DIRECTION('ref_axis',(0.,0.,1.));
#7326=DIRECTION('center_axis',(0.,1.,0.));
#7327=DIRECTION('ref_axis',(1.,0.,0.));
#8820=CARTESIAN_POINT('',(0.,0.,0.));
#8821=CARTESIAN_POINT('Origin',(0.,-1.935,0.));
#8822=CARTESIAN_POINT('',(-0.3933,-3.9267,4.81653586104654E-17));
#8823=CARTESIAN_POINT('Origin',(0.,-3.9267,0.));
#8824=CARTESIAN_POINT('',(-0.3933,0.,-4.81653586104654E-17));
#8825=CARTESIAN_POINT('',(-0.3933,-1.935,-4.81653586104654E-17));
#8826=CARTESIAN_POINT('Origin',(0.,0.,0.));
#8827=CARTESIAN_POINT('Origin',(0.,-3.96,0.));
#8828=CARTESIAN_POINT('',(-0.32,-4.,-3.91886975727153E-17));
#8829=CARTESIAN_POINT('Origin',(0.,-4.,0.));
#8830=CARTESIAN_POINT('',(-0.36,-3.96,-4.40872847693047E-17));
#8831=CARTESIAN_POINT('Origin',(0.,-4.,0.));
#8832=CARTESIAN_POINT('Origin',(0.,0.462722715486149,0.));
#8833=CARTESIAN_POINT('',(-0.6175,0.53,-7.5621939847349E-17));
#8834=CARTESIAN_POINT('Origin',(0.,0.53,0.));
#8835=CARTESIAN_POINT('',(-0.750555349946514,0.453180457891261,-9.19165206894919E-17));
#8836=CARTESIAN_POINT('',(-0.734027674973257,0.462722715486149,-8.98924642641573E-17));
#8837=CARTESIAN_POINT('',(-0.375277674973257,0.453180457891261,0.65));
#8838=CARTESIAN_POINT('Ctrl Pts',(-0.375277674973257,0.45318045789126,0.65));
#8839=CARTESIAN_POINT('Ctrl Pts',(-0.562916512459968,0.561513791224244,
0.324999999999856));
#8840=CARTESIAN_POINT('Ctrl Pts',(-0.750555349946514,0.45318045789126,-9.19165206894919E-17));
#8841=CARTESIAN_POINT('',(0.375277674973257,0.453180457891261,0.65));
#8842=CARTESIAN_POINT('Ctrl Pts',(0.375277674973257,0.453180457891261,0.65));
#8843=CARTESIAN_POINT('Ctrl Pts',(-1.66922031752392E-13,0.561513791224244,
0.65));
#8844=CARTESIAN_POINT('Ctrl Pts',(-0.375277674973257,0.45318045789126,0.65));
#8845=CARTESIAN_POINT('',(0.750555349946514,0.453180457891261,0.));
#8846=CARTESIAN_POINT('Ctrl Pts',(0.750555349946514,0.453180457891261,0.));
#8847=CARTESIAN_POINT('Ctrl Pts',(0.562916512459802,0.561513791224244,0.325000000000144));
#8848=CARTESIAN_POINT('Ctrl Pts',(0.375277674973257,0.45318045789126,0.65));
#8849=CARTESIAN_POINT('',(0.375277674973257,0.453180457891261,-0.65));
#8850=CARTESIAN_POINT('Ctrl Pts',(0.375277674973257,0.45318045789126,-0.65));
#8851=CARTESIAN_POINT('Ctrl Pts',(0.562916512459968,0.561513791224244,-0.324999999999855));
#8852=CARTESIAN_POINT('Ctrl Pts',(0.750555349946514,0.453180457891261,0.));
#8853=CARTESIAN_POINT('',(-0.375277674973257,0.45318045789126,-0.65));
#8854=CARTESIAN_POINT('Ctrl Pts',(-0.375277674973257,0.453180457891261,
-0.65));
#8855=CARTESIAN_POINT('Ctrl Pts',(1.66866520601161E-13,0.561513791224244,
-0.65));
#8856=CARTESIAN_POINT('Ctrl Pts',(0.375277674973257,0.45318045789126,-0.65));
#8857=CARTESIAN_POINT('Ctrl Pts',(-0.750555349946514,0.453180457891261,
-9.19165206894919E-17));
#8858=CARTESIAN_POINT('Ctrl Pts',(-0.562916512459802,0.561513791224244,
-0.325000000000144));
#8859=CARTESIAN_POINT('Ctrl Pts',(-0.375277674973257,0.45318045789126,-0.65));
#8860=CARTESIAN_POINT('Origin',(0.375277674973257,0.,-0.65));
#8861=CARTESIAN_POINT('',(0.375277674973257,0.,-0.65));
#8862=CARTESIAN_POINT('',(0.375277674973257,0.,-0.65));
#8863=CARTESIAN_POINT('',(-0.375277674973257,0.,-0.65));
#8864=CARTESIAN_POINT('',(0.375277674973257,0.,-0.65));
#8865=CARTESIAN_POINT('',(-0.375277674973257,0.,-0.65));
#8866=CARTESIAN_POINT('Origin',(0.750555349946514,0.,0.));
#8867=CARTESIAN_POINT('',(0.750555349946514,0.,0.));
#8868=CARTESIAN_POINT('',(0.750555349946514,0.,0.));
#8869=CARTESIAN_POINT('',(0.750555349946514,0.,0.));
#8870=CARTESIAN_POINT('Origin',(0.375277674973257,0.,0.65));
#8871=CARTESIAN_POINT('',(0.375277674973257,0.,0.65));
#8872=CARTESIAN_POINT('',(0.375277674973257,0.,0.65));
#8873=CARTESIAN_POINT('',(0.375277674973257,0.,0.65));
#8874=CARTESIAN_POINT('Origin',(-0.375277674973257,0.,0.65));
#8875=CARTESIAN_POINT('',(-0.375277674973257,0.,0.65));
#8876=CARTESIAN_POINT('',(-0.375277674973257,0.,0.65));
#8877=CARTESIAN_POINT('',(-0.375277674973257,0.,0.65));
#8878=CARTESIAN_POINT('Origin',(-0.750555349946514,0.,-9.19165206894919E-17));
#8879=CARTESIAN_POINT('',(-0.750555349946514,0.,-9.19165206894919E-17));
#8880=CARTESIAN_POINT('',(-0.750555349946514,0.,-9.19165206894919E-17));
#8881=CARTESIAN_POINT('',(-0.750555349946514,0.,-9.19165206894919E-17));
#8882=CARTESIAN_POINT('Origin',(-0.375277674973257,0.,-0.65));
#8883=CARTESIAN_POINT('',(-0.375277674973257,0.,-0.65));
#8884=CARTESIAN_POINT('Origin',(0.,0.53,-1.11022302462516E-16));
#8885=CARTESIAN_POINT('Origin',(0.,0.,-1.11022302462516E-16));
#9248=UNCERTAINTY_MEASURE_WITH_UNIT(LENGTH_MEASURE(0.001),#9286,
'DISTANCE_ACCURACY_VALUE',
'Maximum model space distance between geometric entities at asserted c
onnectivities');
#9255=UNCERTAINTY_MEASURE_WITH_UNIT(LENGTH_MEASURE(0.001),#9286,
'DISTANCE_ACCURACY_VALUE',
'Maximum model space distance between geometric entities at asserted c
onnectivities');
#9278=(
GEOMETRIC_REPRESENTATION_CONTEXT(3)
GLOBAL_UNCERTAINTY_ASSIGNED_CONTEXT((#9248))
GLOBAL_UNIT_ASSIGNED_CONTEXT((#9286,#9288,#9289))
REPRESENTATION_CONTEXT('','3D')
);
#9285=(
GEOMETRIC_REPRESENTATION_CONTEXT(3)
GLOBAL_UNCERTAINTY_ASSIGNED_CONTEXT((#9255))
GLOBAL_UNIT_ASSIGNED_CONTEXT((#9286,#9288,#9289))
REPRESENTATION_CONTEXT('','3D')
);
#9286=(
LENGTH_UNIT()
NAMED_UNIT(*)
SI_UNIT(.CENTI.,.METRE.)
);
#9288=(
NAMED_UNIT(*)
PLANE_ANGLE_UNIT()
SI_UNIT($,.RADIAN.)
);
#9289=(
NAMED_UNIT(*)
SI_UNIT($,.STERADIAN.)
SOLID_ANGLE_UNIT()
);
#9312=SHAPE_DEFINITION_REPRESENTATION(#9342,#9416);
#9342=PRODUCT_DEFINITION_SHAPE('',$,#9446);
#9416=SHAPE_REPRESENTATION('',(#5901),#9278);
#9423=PRODUCT_DEFINITION_CONTEXT('part definition',#9512,'design');
#9446=PRODUCT_DEFINITION('Hex Bolt - M8x40','Hex Bolt - M8x40',#9475,#9423);
#9475=PRODUCT_DEFINITION_FORMATION('',$,#9536);
#9512=APPLICATION_CONTEXT(
'Core Data for Automotive Mechanical Design Process');
#9513=PRODUCT_CONTEXT('part definition',#9512,'mechanical');
#9536=PRODUCT('Hex Bolt - M8x40','Hex Bolt - M8x40','Hex Bolt - M8x40',
(#9513));
#9613=COLOUR_RGB('Black',0.12,0.14,0.17);
#9614=FILL_AREA_STYLE_COLOUR('',#9613);
#9615=FILL_AREA_STYLE('',(#9614));
#9616=SURFACE_STYLE_FILL_AREA(#9615);
#9617=SURFACE_SIDE_STYLE('',(#9616));
#9618=SURFACE_STYLE_USAGE(.BOTH.,#9617);
#9619=PRESENTATION_STYLE_ASSIGNMENT((#9618));
ENDSEC;
END-ISO-10303-21;
